ISO-10303-21;
HEADER;
/* Generated by software containing ST-Developer
 * from STEP Tools, Inc. (www.steptools.com) 
 */

FILE_DESCRIPTION(
/* description */ ('STEP AP214'),
/* implementation_level */ '2;1');

FILE_NAME(
/* name */ 'M5 Bolt.step',
/* time_stamp */ '2026-10-05T13:15:56-07:00',
/* author */ (''),
/* organization */ (''),
/* preprocessor_version */ 'ST-DEVELOPER v20.2',
/* originating_system */ 'Autodesk Translation Framework v15.15.0.0',
/* authorisation */ '');

FILE_SCHEMA (('AUTOMOTIVE_DESIGN { 1 0 10303 214 3 1 1 }'));
ENDSEC;

DATA;
#10=MECHANICAL_DESIGN_GEOMETRIC_PRESENTATION_REPRESENTATION('',(#1354),#37881);
#1330=SHAPE_REPRESENTATION_RELATIONSHIP('SRR','None',#37963,#1342);
#1342=ADVANCED_BREP_SHAPE_REPRESENTATION('',(#1366),#37878);
#1354=STYLED_ITEM('',(#38023),#1366);
#1366=MANIFOLD_SOLID_BREP('Body1',#10828);
#1462=FACE_BOUND('',#2846,.T.);
#1538=PLANE('',#11814);
#1539=PLANE('',#11815);
#1540=PLANE('',#11816);
#1541=PLANE('',#11817);
#1542=PLANE('',#11818);
#1543=PLANE('',#11819);
#1544=PLANE('',#11820);
#1545=PLANE('',#11821);
#1546=PLANE('',#11822);
#2144=FACE_OUTER_BOUND('',#2838,.T.);
#2145=FACE_OUTER_BOUND('',#2839,.T.);
#2146=FACE_OUTER_BOUND('',#2840,.T.);
#2147=FACE_OUTER_BOUND('',#2841,.T.);
#2148=FACE_OUTER_BOUND('',#2842,.T.);
#2149=FACE_OUTER_BOUND('',#2843,.T.);
#2150=FACE_OUTER_BOUND('',#2844,.T.);
#2151=FACE_OUTER_BOUND('',#2845,.T.);
#2152=FACE_OUTER_BOUND('',#2847,.T.);
#2153=FACE_OUTER_BOUND('',#2848,.T.);
#2838=EDGE_LOOP('',(#9891,#9892,#9893,#9894));
#2839=EDGE_LOOP('',(#9895,#9896,#9897,#9898));
#2840=EDGE_LOOP('',(#9899,#9900,#9901,#9902));
#2841=EDGE_LOOP('',(#9903,#9904,#9905,#9906));
#2842=EDGE_LOOP('',(#9907,#9908,#9909,#9910));
#2843=EDGE_LOOP('',(#9911,#9912,#9913,#9914));
#2844=EDGE_LOOP('',(#9915,#9916,#9917,#9918));
#2845=EDGE_LOOP('',(#9919,#9920,#9921,#9922,#9923,#9924));
#2846=EDGE_LOOP('',(#9925));
#2847=EDGE_LOOP('',(#9926,#9927,#9928,#9929,#9930,#9931));
#2848=EDGE_LOOP('',(#9932));
#3109=LINE('',#37670,#3410);
#3110=LINE('',#37675,#3411);
#3111=LINE('',#37677,#3412);
#3112=LINE('',#37679,#3413);
#3113=LINE('',#37680,#3414);
#3114=LINE('',#37683,#3415);
#3115=LINE('',#37685,#3416);
#3116=LINE('',#37686,#3417);
#3117=LINE('',#37689,#3418);
#3118=LINE('',#37691,#3419);
#3119=LINE('',#37692,#3420);
#3120=LINE('',#37695,#3421);
#3121=LINE('',#37697,#3422);
#3122=LINE('',#37698,#3423);
#3123=LINE('',#37701,#3424);
#3124=LINE('',#37703,#3425);
#3125=LINE('',#37704,#3426);
#3126=LINE('',#37706,#3427);
#3127=LINE('',#37707,#3428);
#3410=VECTOR('',#13826,2.5);
#3411=VECTOR('',#13831,1000.);
#3412=VECTOR('',#13832,1000.);
#3413=VECTOR('',#13833,1000.);
#3414=VECTOR('',#13834,1000.);
#3415=VECTOR('',#13837,1000.);
#3416=VECTOR('',#13838,1000.);
#3417=VECTOR('',#13839,1000.);
#3418=VECTOR('',#13842,1000.);
#3419=VECTOR('',#13843,1000.);
#3420=VECTOR('',#13844,1000.);
#3421=VECTOR('',#13847,1000.);
#3422=VECTOR('',#13848,1000.);
#3423=VECTOR('',#13849,1000.);
#3424=VECTOR('',#13852,1000.);
#3425=VECTOR('',#13853,1000.);
#3426=VECTOR('',#13854,1000.);
#3427=VECTOR('',#13857,1000.);
#3428=VECTOR('',#13858,1000.);
#3992=CIRCLE('',#11812,2.5);
#3993=CIRCLE('',#11813,2.5);
#5027=VERTEX_POINT('',#37667);
#5028=VERTEX_POINT('',#37669);
#5029=VERTEX_POINT('',#37673);
#5030=VERTEX_POINT('',#37674);
#5031=VERTEX_POINT('',#37676);
#5032=VERTEX_POINT('',#37678);
#5033=VERTEX_POINT('',#37682);
#5034=VERTEX_POINT('',#37684);
#5035=VERTEX_POINT('',#37688);
#5036=VERTEX_POINT('',#37690);
#5037=VERTEX_POINT('',#37694);
#5038=VERTEX_POINT('',#37696);
#5039=VERTEX_POINT('',#37700);
#5040=VERTEX_POINT('',#37702);
#6656=EDGE_CURVE('',#5027,#5027,#3992,.T.);
#6657=EDGE_CURVE('',#5027,#5028,#3109,.T.);
#6658=EDGE_CURVE('',#5028,#5028,#3993,.T.);
#6659=EDGE_CURVE('',#5029,#5030,#3110,.T.);
#6660=EDGE_CURVE('',#5031,#5029,#3111,.T.);
#6661=EDGE_CURVE('',#5031,#5032,#3112,.T.);
#6662=EDGE_CURVE('',#5032,#5030,#3113,.T.);
#6663=EDGE_CURVE('',#5033,#5029,#3114,.T.);
#6664=EDGE_CURVE('',#5034,#5033,#3115,.T.);
#6665=EDGE_CURVE('',#5034,#5031,#3116,.T.);
#6666=EDGE_CURVE('',#5035,#5033,#3117,.T.);
#6667=EDGE_CURVE('',#5036,#5035,#3118,.T.);
#6668=EDGE_CURVE('',#5036,#5034,#3119,.T.);
#6669=EDGE_CURVE('',#5037,#5035,#3120,.T.);
#6670=EDGE_CURVE('',#5038,#5037,#3121,.T.);
#6671=EDGE_CURVE('',#5038,#5036,#3122,.T.);
#6672=EDGE_CURVE('',#5039,#5037,#3123,.T.);
#6673=EDGE_CURVE('',#5040,#5039,#3124,.T.);
#6674=EDGE_CURVE('',#5040,#5038,#3125,.T.);
#6675=EDGE_CURVE('',#5030,#5039,#3126,.T.);
#6676=EDGE_CURVE('',#5032,#5040,#3127,.T.);
#9891=ORIENTED_EDGE('',*,*,#6656,.T.);
#9892=ORIENTED_EDGE('',*,*,#6657,.T.);
#9893=ORIENTED_EDGE('',*,*,#6658,.F.);
#9894=ORIENTED_EDGE('',*,*,#6657,.F.);
#9895=ORIENTED_EDGE('',*,*,#6659,.F.);
#9896=ORIENTED_EDGE('',*,*,#6660,.F.);
#9897=ORIENTED_EDGE('',*,*,#6661,.T.);
#9898=ORIENTED_EDGE('',*,*,#6662,.T.);
#9899=ORIENTED_EDGE('',*,*,#6663,.F.);
#9900=ORIENTED_EDGE('',*,*,#6664,.F.);
#9901=ORIENTED_EDGE('',*,*,#6665,.T.);
#9902=ORIENTED_EDGE('',*,*,#6660,.T.);
#9903=ORIENTED_EDGE('',*,*,#6666,.F.);
#9904=ORIENTED_EDGE('',*,*,#6667,.F.);
#9905=ORIENTED_EDGE('',*,*,#6668,.T.);
#9906=ORIENTED_EDGE('',*,*,#6664,.T.);
#9907=ORIENTED_EDGE('',*,*,#6669,.F.);
#9908=ORIENTED_EDGE('',*,*,#6670,.F.);
#9909=ORIENTED_EDGE('',*,*,#6671,.T.);
#9910=ORIENTED_EDGE('',*,*,#6667,.T.);
#9911=ORIENTED_EDGE('',*,*,#6672,.F.);
#9912=ORIENTED_EDGE('',*,*,#6673,.F.);
#9913=ORIENTED_EDGE('',*,*,#6674,.T.);
#9914=ORIENTED_EDGE('',*,*,#6670,.T.);
#9915=ORIENTED_EDGE('',*,*,#6675,.F.);
#9916=ORIENTED_EDGE('',*,*,#6662,.F.);
#9917=ORIENTED_EDGE('',*,*,#6676,.T.);
#9918=ORIENTED_EDGE('',*,*,#6673,.T.);
#9919=ORIENTED_EDGE('',*,*,#6661,.F.);
#9920=ORIENTED_EDGE('',*,*,#6665,.F.);
#9921=ORIENTED_EDGE('',*,*,#6668,.F.);
#9922=ORIENTED_EDGE('',*,*,#6671,.F.);
#9923=ORIENTED_EDGE('',*,*,#6674,.F.);
#9924=ORIENTED_EDGE('',*,*,#6676,.F.);
#9925=ORIENTED_EDGE('',*,*,#6656,.F.);
#9926=ORIENTED_EDGE('',*,*,#6659,.T.);
#9927=ORIENTED_EDGE('',*,*,#6675,.T.);
#9928=ORIENTED_EDGE('',*,*,#6672,.T.);
#9929=ORIENTED_EDGE('',*,*,#6669,.T.);
#9930=ORIENTED_EDGE('',*,*,#6666,.T.);
#9931=ORIENTED_EDGE('',*,*,#6663,.T.);
#9932=ORIENTED_EDGE('',*,*,#6658,.T.);
#10207=CYLINDRICAL_SURFACE('',#11811,2.5);
#10789=ADVANCED_FACE('',(#2144),#10207,.T.);
#10790=ADVANCED_FACE('',(#2145),#1538,.T.);
#10791=ADVANCED_FACE('',(#2146),#1539,.T.);
#10792=ADVANCED_FACE('',(#2147),#1540,.T.);
#10793=ADVANCED_FACE('',(#2148),#1541,.T.);
#10794=ADVANCED_FACE('',(#2149),#1542,.T.);
#10795=ADVANCED_FACE('',(#2150),#1543,.T.);
#10796=ADVANCED_FACE('',(#2151,#1462),#1544,.F.);
#10797=ADVANCED_FACE('',(#2152),#1545,.T.);
#10798=ADVANCED_FACE('',(#2153),#1546,.T.);
#10828=CLOSED_SHELL('',(#10789,#10790,#10791,#10792,#10793,#10794,#10795,
#10796,#10797,#10798));
#11810=AXIS2_PLACEMENT_3D('',#37665,#13820,#13821);
#11811=AXIS2_PLACEMENT_3D('',#37666,#13822,#13823);
#11812=AXIS2_PLACEMENT_3D('',#37668,#13824,#13825);
#11813=AXIS2_PLACEMENT_3D('',#37671,#13827,#13828);
#11814=AXIS2_PLACEMENT_3D('',#37672,#13829,#13830);
#11815=AXIS2_PLACEMENT_3D('',#37681,#13835,#13836);
#11816=AXIS2_PLACEMENT_3D('',#37687,#13840,#13841);
#11817=AXIS2_PLACEMENT_3D('',#37693,#13845,#13846);
#11818=AXIS2_PLACEMENT_3D('',#37699,#13850,#13851);
#11819=AXIS2_PLACEMENT_3D('',#37705,#13855,#13856);
#11820=AXIS2_PLACEMENT_3D('',#37708,#13859,#13860);
#11821=AXIS2_PLACEMENT_3D('',#37709,#13861,#13862);
#11822=AXIS2_PLACEMENT_3D('',#37710,#13863,#13864);
#13820=DIRECTION('axis',(0.,0.,1.));
#13821=DIRECTION('refdir',(1.,0.,0.));
#13822=DIRECTION('center_axis',(0.,0.,1.));
#13823=DIRECTION('ref_axis',(1.,0.,0.));
#13824=DIRECTION('center_axis',(0.,0.,-1.));
#13825=DIRECTION('ref_axis',(-1.,0.,0.));
#13826=DIRECTION('',(0.,0.,-1.));
#13827=DIRECTION('center_axis',(0.,0.,-1.));
#13828=DIRECTION('ref_axis',(-1.,0.,0.));
#13829=DIRECTION('center_axis',(1.,-1.87789324842145E-16,0.));
#13830=DIRECTION('ref_axis',(1.87789324842145E-16,1.,0.));
#13831=DIRECTION('',(1.87789324842145E-16,1.,0.));
#13832=DIRECTION('',(0.,0.,1.));
#13833=DIRECTION('',(1.87789324842145E-16,1.,0.));
#13834=DIRECTION('',(0.,0.,1.));
#13835=DIRECTION('center_axis',(0.5,-0.866025403784439,0.));
#13836=DIRECTION('ref_axis',(0.866025403784439,0.5,0.));
#13837=DIRECTION('',(0.866025403784439,0.5,0.));
#13838=DIRECTION('',(0.,0.,1.));
#13839=DIRECTION('',(0.866025403784439,0.5,0.));
#13840=DIRECTION('center_axis',(-0.5,-0.866025403784439,0.));
#13841=DIRECTION('ref_axis',(0.866025403784439,-0.5,0.));
#13842=DIRECTION('',(0.866025403784438,-0.5,0.));
#13843=DIRECTION('',(0.,0.,1.));
#13844=DIRECTION('',(0.866025403784438,-0.5,0.));
#13845=DIRECTION('center_axis',(-1.,0.,0.));
#13846=DIRECTION('ref_axis',(0.,0.,1.));
#13847=DIRECTION('',(0.,-1.,0.));
#13848=DIRECTION('',(0.,0.,1.));
#13849=DIRECTION('',(0.,-1.,0.));
#13850=DIRECTION('center_axis',(-0.5,0.866025403784439,0.));
#13851=DIRECTION('ref_axis',(-0.866025403784439,-0.5,0.));
#13852=DIRECTION('',(-0.866025403784439,-0.5,0.));
#13853=DIRECTION('',(0.,0.,1.));
#13854=DIRECTION('',(-0.866025403784439,-0.5,0.));
#13855=DIRECTION('center_axis',(0.5,0.866025403784439,0.));
#13856=DIRECTION('ref_axis',(-0.866025403784439,0.5,0.));
#13857=DIRECTION('',(-0.866025403784439,0.5,0.));
#13858=DIRECTION('',(-0.866025403784439,0.5,0.));
#13859=DIRECTION('center_axis',(0.,0.,1.));
#13860=DIRECTION('ref_axis',(1.,0.,0.));
#13861=DIRECTION('center_axis',(0.,0.,1.));
#13862=DIRECTION('ref_axis',(1.,0.,0.));
#13863=DIRECTION('center_axis',(0.,0.,-1.));
#13864=DIRECTION('ref_axis',(-1.,0.,0.));
#37665=CARTESIAN_POINT('',(0.,0.,0.));
#37666=CARTESIAN_POINT('Origin',(0.,0.,-18.5));
#37667=CARTESIAN_POINT('',(-2.5,-3.06161699786838E-16,-3.5));
#37668=CARTESIAN_POINT('Origin',(0.,0.,-3.5));
#37669=CARTESIAN_POINT('',(-2.5,-3.06161699786838E-16,-18.5));
#37670=CARTESIAN_POINT('',(-2.5,-3.06161699786838E-16,-18.5));
#37671=CARTESIAN_POINT('Origin',(0.,0.,-18.5));
#37672=CARTESIAN_POINT('Origin',(4.,-2.3094010767585,-3.5));
#37673=CARTESIAN_POINT('',(4.,-2.3094010767585,0.));
#37674=CARTESIAN_POINT('',(4.,2.3094010767585,0.));
#37675=CARTESIAN_POINT('',(4.,-2.3094010767585,0.));
#37676=CARTESIAN_POINT('',(4.,-2.3094010767585,-3.5));
#37677=CARTESIAN_POINT('',(4.,-2.3094010767585,-3.5));
#37678=CARTESIAN_POINT('',(4.,2.3094010767585,-3.5));
#37679=CARTESIAN_POINT('',(4.,-2.3094010767585,-3.5));
#37680=CARTESIAN_POINT('',(4.,2.3094010767585,-3.5));
#37681=CARTESIAN_POINT('Origin',(3.25260651745651E-16,-4.61880215351701,
-3.5));
#37682=CARTESIAN_POINT('',(3.25260651745651E-16,-4.61880215351701,0.));
#37683=CARTESIAN_POINT('',(3.25260651745651E-16,-4.61880215351701,0.));
#37684=CARTESIAN_POINT('',(3.25260651745651E-16,-4.61880215351701,-3.5));
#37685=CARTESIAN_POINT('',(3.25260651745651E-16,-4.61880215351701,-3.5));
#37686=CARTESIAN_POINT('',(3.25260651745651E-16,-4.61880215351701,-3.5));
#37687=CARTESIAN_POINT('Origin',(-4.,-2.3094010767585,-3.5));
#37688=CARTESIAN_POINT('',(-4.,-2.3094010767585,0.));
#37689=CARTESIAN_POINT('',(-4.,-2.3094010767585,0.));
#37690=CARTESIAN_POINT('',(-4.,-2.3094010767585,-3.5));
#37691=CARTESIAN_POINT('',(-4.,-2.3094010767585,-3.5));
#37692=CARTESIAN_POINT('',(-4.,-2.3094010767585,-3.5));
#37693=CARTESIAN_POINT('Origin',(-4.,2.3094010767585,-3.5));
#37694=CARTESIAN_POINT('',(-4.,2.3094010767585,0.));
#37695=CARTESIAN_POINT('',(-4.,2.3094010767585,0.));
#37696=CARTESIAN_POINT('',(-4.,2.3094010767585,-3.5));
#37697=CARTESIAN_POINT('',(-4.,2.3094010767585,-3.5));
#37698=CARTESIAN_POINT('',(-4.,2.3094010767585,-3.5));
#37699=CARTESIAN_POINT('Origin',(0.,4.61880215351701,-3.5));
#37700=CARTESIAN_POINT('',(0.,4.61880215351701,0.));
#37701=CARTESIAN_POINT('',(0.,4.61880215351701,0.));
#37702=CARTESIAN_POINT('',(0.,4.61880215351701,-3.5));
#37703=CARTESIAN_POINT('',(0.,4.61880215351701,-3.5));
#37704=CARTESIAN_POINT('',(0.,4.61880215351701,-3.5));
#37705=CARTESIAN_POINT('Origin',(4.,2.3094010767585,-3.5));
#37706=CARTESIAN_POINT('',(4.,2.3094010767585,0.));
#37707=CARTESIAN_POINT('',(4.,2.3094010767585,-3.5));
#37708=CARTESIAN_POINT('Origin',(0.,0.,-3.5));
#37709=CARTESIAN_POINT('Origin',(0.,0.,0.));
#37710=CARTESIAN_POINT('Origin',(0.,0.,-18.5));
#37864=UNCERTAINTY_MEASURE_WITH_UNIT(LENGTH_MEASURE(0.01),#37882,
'DISTANCE_ACCURACY_VALUE',
'Maximum model space distance between geometric entities at asserted c
onnectivities');
#37867=UNCERTAINTY_MEASURE_WITH_UNIT(LENGTH_MEASURE(0.01),#37882,
'DISTANCE_ACCURACY_VALUE',
'Maximum model space distance between geometric entities at asserted c
onnectivities');
#37878=(
GEOMETRIC_REPRESENTATION_CONTEXT(3)
GLOBAL_UNCERTAINTY_ASSIGNED_CONTEXT((#37864))
GLOBAL_UNIT_ASSIGNED_CONTEXT((#37882,#37884,#37885))
REPRESENTATION_CONTEXT('','3D')
);
#37881=(
GEOMETRIC_REPRESENTATION_CONTEXT(3)
GLOBAL_UNCERTAINTY_ASSIGNED_CONTEXT((#37867))
GLOBAL_UNIT_ASSIGNED_CONTEXT((#37882,#37884,#37885))
REPRESENTATION_CONTEXT('','3D')
);
#37882=(
LENGTH_UNIT()
NAMED_UNIT(*)
SI_UNIT(.MILLI.,.METRE.)
);
#37884=(
NAMED_UNIT(*)
PLANE_ANGLE_UNIT()
SI_UNIT($,.RADIAN.)
);
#37885=(
NAMED_UNIT(*)
SI_UNIT($,.STERADIAN.)
SOLID_ANGLE_UNIT()
);
#37896=SHAPE_DEFINITION_REPRESENTATION(#37909,#37963);
#37909=PRODUCT_DEFINITION_SHAPE('',$,#37977);
#37963=SHAPE_REPRESENTATION('',(#11810),#37878);
#37966=PRODUCT_DEFINITION_CONTEXT('part definition',#38007,'design');
#37977=PRODUCT_DEFINITION('PS11','M5 Bolt',#37990,#37966);
#37990=PRODUCT_DEFINITION_FORMATION('',$,#38019);
#38007=APPLICATION_CONTEXT(
'Core Data for Automotive Mechanical Design Process');
#38008=PRODUCT_CONTEXT('part definition',#38007,'mechanical');
#38019=PRODUCT('PS11','M5 Bolt',$,(#38008));
#38023=PRESENTATION_STYLE_ASSIGNMENT((#38025));
#38025=SURFACE_STYLE_USAGE(.BOTH.,#38027);
#38027=SURFACE_SIDE_STYLE('',(#38029));
#38029=SURFACE_STYLE_FILL_AREA(#38031);
#38031=FILL_AREA_STYLE('Opaque(202,209,238)',(#38033));
#38033=FILL_AREA_STYLE_COLOUR('Opaque(202,209,238)',#38035);
#38035=COLOUR_RGB('Opaque(202,209,238)', 0.66274510, 0.83137255, 0.94901961);
ENDSEC;
END-ISO-10303-21;
